ISO-10303-21;
HEADER;
/* Generated by software containing ST-Developer
 * from STEP Tools, Inc. (www.steptools.com) 
 */

FILE_DESCRIPTION(
/* description */ ('Bin tilter linkage'),
/* implementation_level */ '2;1');

FILE_NAME(
/* name */ 'Screw keeper fastener (5).step',
/* time_stamp */ '2026-10-28T03:26:24-07:00',
/* author */ (''),
/* organization */ (''),
/* preprocessor_version */ 'ST-DEVELOPER v20.2',
/* originating_system */ 'Autodesk Translation Framework v15.17.0.0',
/* authorisation */ '');

FILE_SCHEMA (('AUTOMOTIVE_DESIGN { 1 0 10303 214 3 1 1 }'));
ENDSEC;

DATA;
#10=MECHANICAL_DESIGN_GEOMETRIC_PRESENTATION_REPRESENTATION('',(#885),#23728);
#673=SHAPE_REPRESENTATION_RELATIONSHIP('SRR','None',#24137,#779);
#779=ADVANCED_BREP_SHAPE_REPRESENTATION('',(#999),#23637);
#885=STYLED_ITEM('',(#24772),#999);
#999=MANIFOLD_SOLID_BREP('Body1',#12415);
#1224=FACE_BOUND('',#3007,.T.);
#1591=PLANE('',#14110);
#1592=PLANE('',#14115);
#1593=PLANE('',#14118);
#2092=FACE_OUTER_BOUND('',#3006,.T.);
#2093=FACE_OUTER_BOUND('',#3008,.T.);
#2094=FACE_OUTER_BOUND('',#3009,.T.);
#2095=FACE_OUTER_BOUND('',#3010,.T.);
#2096=FACE_OUTER_BOUND('',#3011,.T.);
#3006=EDGE_LOOP('',(#9219));
#3007=EDGE_LOOP('',(#9220));
#3008=EDGE_LOOP('',(#9221,#9222,#9223,#9224));
#3009=EDGE_LOOP('',(#9225));
#3010=EDGE_LOOP('',(#9226,#9227,#9228,#9229));
#3011=EDGE_LOOP('',(#9230));
#4066=LINE('',#20685,#4741);
#4067=LINE('',#20691,#4742);
#4741=VECTOR('',#16567,0.35);
#4742=VECTOR('',#16576,0.2);
#5405=CIRCLE('',#14111,0.35);
#5406=CIRCLE('',#14112,0.2);
#5407=CIRCLE('',#14114,0.35);
#5408=CIRCLE('',#14117,0.2);
#6239=VERTEX_POINT('',#20679);
#6240=VERTEX_POINT('',#20681);
#6241=VERTEX_POINT('',#20684);
#6242=VERTEX_POINT('',#20689);
#7349=EDGE_CURVE('',#6239,#6239,#5405,.T.);
#7350=EDGE_CURVE('',#6240,#6240,#5406,.T.);
#7351=EDGE_CURVE('',#6239,#6241,#4066,.T.);
#7352=EDGE_CURVE('',#6241,#6241,#5407,.T.);
#7353=EDGE_CURVE('',#6242,#6242,#5408,.T.);
#7354=EDGE_CURVE('',#6242,#6240,#4067,.T.);
#9219=ORIENTED_EDGE('',*,*,#7349,.T.);
#9220=ORIENTED_EDGE('',*,*,#7350,.F.);
#9221=ORIENTED_EDGE('',*,*,#7349,.F.);
#9222=ORIENTED_EDGE('',*,*,#7351,.T.);
#9223=ORIENTED_EDGE('',*,*,#7352,.T.);
#9224=ORIENTED_EDGE('',*,*,#7351,.F.);
#9225=ORIENTED_EDGE('',*,*,#7352,.F.);
#9226=ORIENTED_EDGE('',*,*,#7353,.F.);
#9227=ORIENTED_EDGE('',*,*,#7354,.T.);
#9228=ORIENTED_EDGE('',*,*,#7350,.T.);
#9229=ORIENTED_EDGE('',*,*,#7354,.F.);
#9230=ORIENTED_EDGE('',*,*,#7353,.T.);
#11370=CYLINDRICAL_SURFACE('',#14113,0.35);
#11371=CYLINDRICAL_SURFACE('',#14116,0.2);
#11817=ADVANCED_FACE('',(#2092,#1224),#1591,.T.);
#11818=ADVANCED_FACE('',(#2093),#11370,.T.);
#11819=ADVANCED_FACE('',(#2094),#1592,.F.);
#11820=ADVANCED_FACE('',(#2095),#11371,.T.);
#11821=ADVANCED_FACE('',(#2096),#1593,.T.);
#12415=CLOSED_SHELL('',(#11817,#11818,#11819,#11820,#11821));
#14109=AXIS2_PLACEMENT_3D('',#20677,#16557,#16558);
#14110=AXIS2_PLACEMENT_3D('',#20678,#16559,#16560);
#14111=AXIS2_PLACEMENT_3D('',#20680,#16561,#16562);
#14112=AXIS2_PLACEMENT_3D('',#20682,#16563,#16564);
#14113=AXIS2_PLACEMENT_3D('',#20683,#16565,#16566);
#14114=AXIS2_PLACEMENT_3D('',#20686,#16568,#16569);
#14115=AXIS2_PLACEMENT_3D('',#20687,#16570,#16571);
#14116=AXIS2_PLACEMENT_3D('',#20688,#16572,#16573);
#14117=AXIS2_PLACEMENT_3D('',#20690,#16574,#16575);
#14118=AXIS2_PLACEMENT_3D('',#20692,#16577,#16578);
#16557=DIRECTION('axis',(0.,0.,1.));
#16558=DIRECTION('refdir',(1.,0.,0.));
#16559=DIRECTION('center_axis',(1.,0.,0.));
#16560=DIRECTION('ref_axis',(0.,0.,-1.));
#16561=DIRECTION('center_axis',(1.,0.,0.));
#16562=DIRECTION('ref_axis',(0.,0.,-1.));
#16563=DIRECTION('center_axis',(1.,0.,0.));
#16564=DIRECTION('ref_axis',(0.,0.,-1.));
#16565=DIRECTION('center_axis',(1.,0.,0.));
#16566=DIRECTION('ref_axis',(0.,0.,-1.));
#16567=DIRECTION('',(-1.,0.,0.));
#16568=DIRECTION('center_axis',(1.,0.,0.));
#16569=DIRECTION('ref_axis',(0.,0.,-1.));
#16570=DIRECTION('center_axis',(1.,0.,0.));
#16571=DIRECTION('ref_axis',(0.,0.,-1.));
#16572=DIRECTION('center_axis',(1.,0.,0.));
#16573=DIRECTION('ref_axis',(0.,0.,-1.));
#16574=DIRECTION('center_axis',(1.,0.,0.));
#16575=DIRECTION('ref_axis',(0.,0.,-1.));
#16576=DIRECTION('',(-1.,0.,0.));
#16577=DIRECTION('center_axis',(1.,0.,0.));
#16578=DIRECTION('ref_axis',(0.,0.,-1.));
#20677=CARTESIAN_POINT('',(0.,0.,0.));
#20678=CARTESIAN_POINT('Origin',(-0.2,-4.5,6.15));
#20679=CARTESIAN_POINT('',(-0.2,-4.5,6.5));
#20680=CARTESIAN_POINT('Origin',(-0.2,-4.5,6.15));
#20681=CARTESIAN_POINT('',(-0.2,-4.5,6.35));
#20682=CARTESIAN_POINT('Origin',(-0.2,-4.5,6.15));
#20683=CARTESIAN_POINT('Origin',(-0.6,-4.5,6.15));
#20684=CARTESIAN_POINT('',(-0.6,-4.5,6.5));
#20685=CARTESIAN_POINT('',(-0.6,-4.5,6.5));
#20686=CARTESIAN_POINT('Origin',(-0.6,-4.5,6.15));
#20687=CARTESIAN_POINT('Origin',(-0.6,-4.5,6.15));
#20688=CARTESIAN_POINT('Origin',(-0.2,-4.5,6.15));
#20689=CARTESIAN_POINT('',(0.5,-4.5,6.35));
#20690=CARTESIAN_POINT('Origin',(0.5,-4.5,6.15));
#20691=CARTESIAN_POINT('',(-0.2,-4.5,6.35));
#20692=CARTESIAN_POINT('Origin',(0.5,-4.5,6.15));
#23520=UNCERTAINTY_MEASURE_WITH_UNIT(LENGTH_MEASURE(0.001),#23729,
'DISTANCE_ACCURACY_VALUE',
'Maximum model space distance between geometric entities at asserted c
onnectivities');
#23611=UNCERTAINTY_MEASURE_WITH_UNIT(LENGTH_MEASURE(0.001),#23729,
'DISTANCE_ACCURACY_VALUE',
'Maximum model space distance between geometric entities at asserted c
onnectivities');
#23637=(
GEOMETRIC_REPRESENTATION_CONTEXT(3)
GLOBAL_UNCERTAINTY_ASSIGNED_CONTEXT((#23520))
GLOBAL_UNIT_ASSIGNED_CONTEXT((#23729,#23731,#23732))
REPRESENTATION_CONTEXT('','3D')
);
#23728=(
GEOMETRIC_REPRESENTATION_CONTEXT(3)
GLOBAL_UNCERTAINTY_ASSIGNED_CONTEXT((#23611))
GLOBAL_UNIT_ASSIGNED_CONTEXT((#23729,#23731,#23732))
REPRESENTATION_CONTEXT('','3D')
);
#23729=(
LENGTH_UNIT()
NAMED_UNIT(*)
SI_UNIT(.CENTI.,.METRE.)
);
#23731=(
NAMED_UNIT(*)
PLANE_ANGLE_UNIT()
SI_UNIT($,.RADIAN.)
);
#23732=(
NAMED_UNIT(*)
SI_UNIT($,.STERADIAN.)
SOLID_ANGLE_UNIT()
);
#23758=SHAPE_DEFINITION_REPRESENTATION(#23874,#24137);
#23874=PRODUCT_DEFINITION_SHAPE('',$,#24254);
#24137=SHAPE_REPRESENTATION('',(#14109),#23637);
#24228=PRODUCT_DEFINITION_CONTEXT('part definition',#24578,'design');
#24254=PRODUCT_DEFINITION('Screw keeper fastener (5)',
'Screw keeper fastener (5)',#24370,#24228);
#24370=PRODUCT_DEFINITION_FORMATION('',$,#24605);
#24578=APPLICATION_CONTEXT(
'Core Data for Automotive Mechanical Design Process');
#24579=PRODUCT_CONTEXT('part definition',#24578,'mechanical');
#24605=PRODUCT('Screw keeper fastener (5)','Screw keeper fastener (5)',
'Screw keeper fastener (5)',(#24579));
#24766=COLOUR_RGB('Black',0.12,0.14,0.17);
#24767=FILL_AREA_STYLE_COLOUR('',#24766);
#24768=FILL_AREA_STYLE('',(#24767));
#24769=SURFACE_STYLE_FILL_AREA(#24768);
#24770=SURFACE_SIDE_STYLE('',(#24769));
#24771=SURFACE_STYLE_USAGE(.BOTH.,#24770);
#24772=PRESENTATION_STYLE_ASSIGNMENT((#24771));
ENDSEC;
END-ISO-10303-21;
